ISO-10303-21;
HEADER;
/* Generated by software containing ST-Developer
 * from STEP Tools, Inc. (www.steptools.com) 
 */

FILE_DESCRIPTION(
/* description */ (''),
/* implementation_level */ '2;1');

FILE_NAME(
/* name */ 'Pin screw.step',
/* time_stamp */ '2026-11-14T09:55:16-08:00',
/* author */ (''),
/* organization */ (''),
/* preprocessor_version */ 'ST-DEVELOPER v20.2',
/* originating_system */ 'Autodesk Translation Framework v15.17.0.0',
/* authorisation */ '');

FILE_SCHEMA (('AUTOMOTIVE_DESIGN { 1 0 10303 214 3 1 1 }'));
ENDSEC;

DATA;
#10=MECHANICAL_DESIGN_GEOMETRIC_PRESENTATION_REPRESENTATION('',(#62),#170250);
#48=SHAPE_REPRESENTATION_RELATIONSHIP('SRR','None',#170280,#54);
#54=ADVANCED_BREP_SHAPE_REPRESENTATION('',(#68),#170248);
#62=STYLED_ITEM('',(#170317),#68);
#68=MANIFOLD_SOLID_BREP('Body1',#71402);
#85=FACE_BOUND('',#15920,.T.);
#108=PLANE('',#77748);
#109=PLANE('',#77749);
#5380=CYLINDRICAL_SURFACE('',#77740,2.5);
#5381=CYLINDRICAL_SURFACE('',#77750,1.676167978);
#10639=FACE_OUTER_BOUND('',#15919,.T.);
#10640=FACE_OUTER_BOUND('',#15921,.T.);
#10641=FACE_OUTER_BOUND('',#15922,.T.);
#10642=FACE_OUTER_BOUND('',#15923,.T.);
#10643=FACE_OUTER_BOUND('',#15924,.T.);
#10644=FACE_OUTER_BOUND('',#15925,.T.);
#15919=EDGE_LOOP('',(#65968,#65969,#65970,#65971,#65972,#65973,#65974,#65975,
#65976,#65977));
#15920=EDGE_LOOP('',(#65978,#65979));
#15921=EDGE_LOOP('',(#65980,#65981,#65982,#65983));
#15922=EDGE_LOOP('',(#65984,#65985,#65986,#65987,#65988));
#15923=EDGE_LOOP('',(#65989));
#15924=EDGE_LOOP('',(#65990));
#15925=EDGE_LOOP('',(#65991,#65992,#65993,#65994,#65995,#65996,#65997));
#21039=CIRCLE('',#77741,2.5);
#21040=CIRCLE('',#77742,2.5);
#21041=CIRCLE('',#77743,2.5);
#21042=CIRCLE('',#77745,2.);
#21043=CIRCLE('',#77747,2.);
#24352=B_SPLINE_CURVE_WITH_KNOTS('',3,(#170120,#170121,#170122,#170123),
 .UNSPECIFIED.,.F.,.F.,(4,4),(1.31298214335883,1.31559438320612),
 .UNSPECIFIED.);
#24353=B_SPLINE_CURVE_WITH_KNOTS('',3,(#170125,#170126,#170127,#170128,
#170129,#170130,#170131,#170132,#170133,#170134,#170135,#170136,#170137,
#170138,#170139,#170140,#170141,#170142,#170143,#170144),.UNSPECIFIED.,
 .F.,.F.,(4,2,2,2,2,2,2,2,2,4),(1.31559438320612,1.3812434679175,1.44689255262887,
1.5131731285367,1.57945370444452,1.64573428035235,1.71201485626017,1.77766394097155,
1.84331302568292,1.84592524876208),.UNSPECIFIED.);
#24354=B_SPLINE_CURVE_WITH_KNOTS('',3,(#170148,#170149,#170150,#170151,
#170152,#170153,#170154,#170155,#170156,#170157,#170158,#170159,#170160,
#170161,#170162,#170163,#170164,#170165,#170166),.UNSPECIFIED.,.F.,.F.,
(4,2,2,2,3,2,2,2,4),(0.792955713409892,0.85556854154341,0.920793592756085,
0.986881564054135,1.05296953535218,1.11898939802791,1.18500926070363,1.25030182195487,
1.31298214335883),.UNSPECIFIED.);
#24355=B_SPLINE_CURVE_WITH_KNOTS('',3,(#170169,#170170,#170171,#170172),
 .UNSPECIFIED.,.F.,.F.,(4,4),(1.84331422285043,1.84592646269772),
 .UNSPECIFIED.);
#24356=B_SPLINE_CURVE_WITH_KNOTS('',3,(#170173,#170174,#170175,#170176,
#170177,#170178,#170179,#170180,#170181,#170182,#170183,#170184,#170185,
#170186,#170187,#170188,#170189,#170190,#170191,#170192,#170193,#170194,
#170195,#170196,#170197,#170198,#170199,#170200,#170201,#170202,#170203,
#170204,#170205,#170206,#170207),.UNSPECIFIED.,.F.,.F.,(4,2,2,2,3,2,2,2,
2,2,2,2,2,2,2,2,4),(0.792956927345539,0.855637248749495,0.920929810000743,
0.986949672676464,1.05296953535218,1.11905750665023,1.18514547794829,1.25037052916096,
1.31559558037363,1.38124466508501,1.44689374979638,1.51317432570421,1.57945490161203,
1.64573547751986,1.71201605342768,1.77766513813906,1.84331422285043),
 .UNSPECIFIED.);
#26439=LINE('',#170118,#28527);
#26440=LINE('',#170146,#28528);
#26441=LINE('',#170210,#28529);
#26442=LINE('',#170214,#28530);
#26443=LINE('',#170219,#28531);
#28527=VECTOR('',#92389,2.5);
#28528=VECTOR('',#92390,2.5);
#28529=VECTOR('',#92395,2.);
#28530=VECTOR('',#92400,2.);
#28531=VECTOR('',#92409,1.676167978);
#33952=VERTEX_POINT('',#170113);
#33953=VERTEX_POINT('',#170114);
#33954=VERTEX_POINT('',#170117);
#33955=VERTEX_POINT('',#170119);
#33956=VERTEX_POINT('',#170124);
#33957=VERTEX_POINT('',#170145);
#33958=VERTEX_POINT('',#170167);
#33959=VERTEX_POINT('',#170168);
#33960=VERTEX_POINT('',#170209);
#33961=VERTEX_POINT('',#170213);
#44628=EDGE_CURVE('',#33952,#33953,#21039,.T.);
#44629=EDGE_CURVE('',#33953,#33952,#21040,.T.);
#44630=EDGE_CURVE('',#33953,#33954,#26439,.T.);
#44631=EDGE_CURVE('',#33955,#33954,#24352,.F.);
#44632=EDGE_CURVE('',#33956,#33955,#24353,.F.);
#44633=EDGE_CURVE('',#33956,#33957,#26440,.T.);
#44634=EDGE_CURVE('',#33957,#33957,#21041,.T.);
#44635=EDGE_CURVE('',#33954,#33956,#24354,.F.);
#44636=EDGE_CURVE('',#33958,#33959,#24355,.F.);
#44637=EDGE_CURVE('',#33959,#33958,#24356,.F.);
#44638=EDGE_CURVE('',#33957,#33960,#26441,.T.);
#44639=EDGE_CURVE('',#33960,#33960,#21042,.T.);
#44640=EDGE_CURVE('',#33952,#33961,#26442,.T.);
#44641=EDGE_CURVE('',#33961,#33961,#21043,.T.);
#44642=EDGE_CURVE('',#33955,#33959,#26443,.T.);
#65968=ORIENTED_EDGE('',*,*,#44628,.F.);
#65969=ORIENTED_EDGE('',*,*,#44629,.F.);
#65970=ORIENTED_EDGE('',*,*,#44630,.T.);
#65971=ORIENTED_EDGE('',*,*,#44631,.F.);
#65972=ORIENTED_EDGE('',*,*,#44632,.F.);
#65973=ORIENTED_EDGE('',*,*,#44633,.T.);
#65974=ORIENTED_EDGE('',*,*,#44634,.F.);
#65975=ORIENTED_EDGE('',*,*,#44633,.F.);
#65976=ORIENTED_EDGE('',*,*,#44635,.F.);
#65977=ORIENTED_EDGE('',*,*,#44630,.F.);
#65978=ORIENTED_EDGE('',*,*,#44636,.F.);
#65979=ORIENTED_EDGE('',*,*,#44637,.F.);
#65980=ORIENTED_EDGE('',*,*,#44634,.T.);
#65981=ORIENTED_EDGE('',*,*,#44638,.T.);
#65982=ORIENTED_EDGE('',*,*,#44639,.F.);
#65983=ORIENTED_EDGE('',*,*,#44638,.F.);
#65984=ORIENTED_EDGE('',*,*,#44628,.T.);
#65985=ORIENTED_EDGE('',*,*,#44629,.T.);
#65986=ORIENTED_EDGE('',*,*,#44640,.T.);
#65987=ORIENTED_EDGE('',*,*,#44641,.F.);
#65988=ORIENTED_EDGE('',*,*,#44640,.F.);
#65989=ORIENTED_EDGE('',*,*,#44641,.T.);
#65990=ORIENTED_EDGE('',*,*,#44639,.T.);
#65991=ORIENTED_EDGE('',*,*,#44632,.T.);
#65992=ORIENTED_EDGE('',*,*,#44642,.T.);
#65993=ORIENTED_EDGE('',*,*,#44637,.T.);
#65994=ORIENTED_EDGE('',*,*,#44636,.T.);
#65995=ORIENTED_EDGE('',*,*,#44642,.F.);
#65996=ORIENTED_EDGE('',*,*,#44631,.T.);
#65997=ORIENTED_EDGE('',*,*,#44635,.T.);
#66131=CONICAL_SURFACE('',#77744,2.,0.785398163397448);
#66132=CONICAL_SURFACE('',#77746,2.,0.785398163397448);
#71389=ADVANCED_FACE('',(#10639,#85),#5380,.T.);
#71390=ADVANCED_FACE('',(#10640),#66131,.T.);
#71391=ADVANCED_FACE('',(#10641),#66132,.T.);
#71392=ADVANCED_FACE('',(#10642),#108,.F.);
#71393=ADVANCED_FACE('',(#10643),#109,.T.);
#71394=ADVANCED_FACE('',(#10644),#5381,.F.);
#71402=CLOSED_SHELL('',(#71389,#71390,#71391,#71392,#71393,#71394));
#77739=AXIS2_PLACEMENT_3D('',#170111,#92381,#92382);
#77740=AXIS2_PLACEMENT_3D('',#170112,#92383,#92384);
#77741=AXIS2_PLACEMENT_3D('',#170115,#92385,#92386);
#77742=AXIS2_PLACEMENT_3D('',#170116,#92387,#92388);
#77743=AXIS2_PLACEMENT_3D('',#170147,#92391,#92392);
#77744=AXIS2_PLACEMENT_3D('',#170208,#92393,#92394);
#77745=AXIS2_PLACEMENT_3D('',#170211,#92396,#92397);
#77746=AXIS2_PLACEMENT_3D('',#170212,#92398,#92399);
#77747=AXIS2_PLACEMENT_3D('',#170215,#92401,#92402);
#77748=AXIS2_PLACEMENT_3D('',#170216,#92403,#92404);
#77749=AXIS2_PLACEMENT_3D('',#170217,#92405,#92406);
#77750=AXIS2_PLACEMENT_3D('',#170218,#92407,#92408);
#92381=DIRECTION('axis',(0.,0.,1.));
#92382=DIRECTION('refdir',(1.,0.,0.));
#92383=DIRECTION('center_axis',(0.,-3.46944695195362E-16,-1.));
#92384=DIRECTION('ref_axis',(0.,1.,-3.46944695195362E-16));
#92385=DIRECTION('center_axis',(2.20309881449055E-14,0.,-1.));
#92386=DIRECTION('ref_axis',(1.,0.,2.20309881449055E-14));
#92387=DIRECTION('center_axis',(2.20309881449055E-14,0.,-1.));
#92388=DIRECTION('ref_axis',(1.,0.,2.20309881449055E-14));
#92389=DIRECTION('',(0.,3.46944695195362E-16,1.));
#92390=DIRECTION('',(0.,3.46944695195362E-16,1.));
#92391=DIRECTION('center_axis',(-2.63677968348475E-14,0.,1.));
#92392=DIRECTION('ref_axis',(-1.,0.,-2.63677968348475E-14));
#92393=DIRECTION('center_axis',(0.,-1.73472347597681E-15,-1.));
#92394=DIRECTION('ref_axis',(0.,1.,-1.73472347597681E-15));
#92395=DIRECTION('',(8.65956056235493E-17,0.707106781186548,0.707106781186547));
#92396=DIRECTION('center_axis',(0.,0.,1.));
#92397=DIRECTION('ref_axis',(-1.,0.,0.));
#92398=DIRECTION('center_axis',(0.,0.,1.));
#92399=DIRECTION('ref_axis',(1.,0.,0.));
#92400=DIRECTION('',(0.707106781186547,8.65956056235493E-17,-0.707106781186548));
#92401=DIRECTION('center_axis',(0.,0.,-1.));
#92402=DIRECTION('ref_axis',(1.,0.,0.));
#92403=DIRECTION('center_axis',(0.,0.,1.));
#92404=DIRECTION('ref_axis',(1.,0.,0.));
#92405=DIRECTION('center_axis',(0.,0.,1.));
#92406=DIRECTION('ref_axis',(1.,0.,0.));
#92407=DIRECTION('center_axis',(-2.20842887353658E-15,1.,-2.20842887397973E-15));
#92408=DIRECTION('ref_axis',(2.65393425879704E-31,2.20842887397973E-15,
1.));
#92409=DIRECTION('',(-2.20842887353658E-15,1.,-2.20842887397973E-15));
#170111=CARTESIAN_POINT('',(0.,0.,0.));
#170112=CARTESIAN_POINT('Origin',(0.,1.53080849893419E-16,11.5));
#170113=CARTESIAN_POINT('',(-2.5,-1.83697019872103E-16,0.5));
#170114=CARTESIAN_POINT('',(-3.06161699786838E-16,-2.5,0.499999999999889));
#170115=CARTESIAN_POINT('Origin',(0.,0.,0.499999999999945));
#170116=CARTESIAN_POINT('Origin',(0.,0.,0.499999999999945));
#170117=CARTESIAN_POINT('',(8.70406000932897E-16,-2.5,4.32403629890143));
#170118=CARTESIAN_POINT('',(-3.06161699786838E-16,-2.5,11.5));
#170119=CARTESIAN_POINT('',(-0.0261679780000105,-2.49986304363407,4.323832022));
#170120=CARTESIAN_POINT('Ctrl Pts',(1.15791230912943E-15,-2.5,4.32403629890143));
#170121=CARTESIAN_POINT('Ctrl Pts',(-0.00873762991264322,-2.5,4.32389987225498));
#170122=CARTESIAN_POINT('Ctrl Pts',(-0.017460988859543,-2.49995418634721,
4.323832022));
#170123=CARTESIAN_POINT('Ctrl Pts',(-0.0261679780000102,-2.49986304363407,
4.323832022));
#170124=CARTESIAN_POINT('',(3.00643086045464E-16,-2.5,7.67596370109857));
#170125=CARTESIAN_POINT('Ctrl Pts',(-0.0261679780000103,-2.49986304363407,
4.323832022));
#170126=CARTESIAN_POINT('Ctrl Pts',(-0.24498627229117,-2.49757250522814,
4.323832022));
#170127=CARTESIAN_POINT('Ctrl Pts',(-0.473268510539816,-2.46408580788035,
4.36919017818471));
#170128=CARTESIAN_POINT('Ctrl Pts',(-0.884756057426636,-2.34795838069478,
4.54320012976031));
#170129=CARTESIAN_POINT('Ctrl Pts',(-1.06835830755763,-2.2662099535775,
4.67150721032226));
#170130=CARTESIAN_POINT('Ctrl Pts',(-1.35766683964857,-2.10579239001524,
4.9612666013408));
#170131=CARTESIAN_POINT('Ctrl Pts',(-1.48440903437883,-2.01464276874608,
5.1443221770531));
#170132=CARTESIAN_POINT('Ctrl Pts',(-1.65667979852069,-1.87554500871045,
5.55269584787951));
#170133=CARTESIAN_POINT('Ctrl Pts',(-1.70233595600002,-1.83086107963153,
5.77906474697392));
#170134=CARTESIAN_POINT('Ctrl Pts',(-1.70233595600002,-1.83086107963153,
6.22093525302608));
#170135=CARTESIAN_POINT('Ctrl Pts',(-1.65667979852069,-1.87554500871045,
6.44730415212049));
#170136=CARTESIAN_POINT('Ctrl Pts',(-1.48440903437883,-2.01464276874608,
6.85567782294691));
#170137=CARTESIAN_POINT('Ctrl Pts',(-1.35766683964857,-2.10579239001524,
7.0387333986592));
#170138=CARTESIAN_POINT('Ctrl Pts',(-1.06835830755763,-2.2662099535775,
7.32849278967774));
#170139=CARTESIAN_POINT('Ctrl Pts',(-0.884756057426636,-2.34795838069478,
7.4567998702397));
#170140=CARTESIAN_POINT('Ctrl Pts',(-0.473268510539817,-2.46408580788035,
7.63080982181529));
#170141=CARTESIAN_POINT('Ctrl Pts',(-0.244986272291171,-2.49757250522814,
7.67616797800001));
#170142=CARTESIAN_POINT('Ctrl Pts',(-0.0174610447502658,-2.49995418576216,
7.67616797800001));
#170143=CARTESIAN_POINT('Ctrl Pts',(-0.00873768451990147,-2.5,7.67610012859765));
#170144=CARTESIAN_POINT('Ctrl Pts',(-8.74711317429465E-16,-2.5,7.67596370109857));
#170145=CARTESIAN_POINT('',(-3.06161699786838E-16,-2.5,11.5000000000001));
#170146=CARTESIAN_POINT('',(-3.06161699786838E-16,-2.5,11.5));
#170147=CARTESIAN_POINT('Origin',(0.,0.,11.5));
#170148=CARTESIAN_POINT('Ctrl Pts',(-1.04083408558608E-15,-2.5,7.67596370109857));
#170149=CARTESIAN_POINT('Ctrl Pts',(0.209435076006717,-2.5,7.67269364670671));
#170150=CARTESIAN_POINT('Ctrl Pts',(0.427069444468387,-2.47166813023646,
7.6278705668994));
#170151=CARTESIAN_POINT('Ctrl Pts',(0.829970933278297,-2.36774524063037,
7.45818999174565));
#170152=CARTESIAN_POINT('Ctrl Pts',(1.01388009229789,-2.29097319034087,
7.33019525229807));
#170153=CARTESIAN_POINT('Ctrl Pts',(1.30438035120315,-2.1391140724923,7.04012885008983));
#170154=CARTESIAN_POINT('Ctrl Pts',(1.43174135154912,-2.05230071367003,
6.85639405508702));
#170155=CARTESIAN_POINT('Ctrl Pts',(1.60451571026846,-1.92024797131867,
6.44696680522558));
#170156=CARTESIAN_POINT('Ctrl Pts',(1.64999999999999,-1.8781639970993,6.22029323766017));
#170157=CARTESIAN_POINT('Ctrl Pts',(1.64999999999999,-1.8781639970993,6.));
#170158=CARTESIAN_POINT('Ctrl Pts',(1.64999999999999,-1.8781639970993,5.77993379108093));
#170159=CARTESIAN_POINT('Ctrl Pts',(1.60460561689047,-1.92016237998017,
5.55346129141823));
#170160=CARTESIAN_POINT('Ctrl Pts',(1.43214140343333,-2.05201177715308,
5.14433951978893));
#170161=CARTESIAN_POINT('Ctrl Pts',(1.30500271214397,-2.13871416924791,
4.96071120284089));
#170162=CARTESIAN_POINT('Ctrl Pts',(1.01472856346469,-2.29060294533492,
4.67043705416161));
#170163=CARTESIAN_POINT('Ctrl Pts',(0.830717428883742,-2.36749905155108,
4.54221720082961));
#170164=CARTESIAN_POINT('Ctrl Pts',(0.42750255255265,-2.47160775999572,
4.37222300033198));
#170165=CARTESIAN_POINT('Ctrl Pts',(0.209658179665775,-2.5,4.32730983676471));
#170166=CARTESIAN_POINT('Ctrl Pts',(1.17961196366423E-15,-2.5,4.32403629890143));
#170167=CARTESIAN_POINT('',(-1.22751689441858E-17,2.5,4.32403629890142));
#170168=CARTESIAN_POINT('',(-0.0261679780000216,2.49986304363407,4.32383202199999));
#170169=CARTESIAN_POINT('Ctrl Pts',(-0.0261679780000214,2.49986304363407,
4.32383202199999));
#170170=CARTESIAN_POINT('Ctrl Pts',(-0.0174609888595512,2.49995418634721,
4.32383202199999));
#170171=CARTESIAN_POINT('Ctrl Pts',(-0.00873762991264853,2.5,4.32389987225497));
#170172=CARTESIAN_POINT('Ctrl Pts',(-1.16462285072049E-15,2.5,4.32403629890142));
#170173=CARTESIAN_POINT('Ctrl Pts',(-1.2490009027033E-15,2.5,4.32403629890142));
#170174=CARTESIAN_POINT('Ctrl Pts',(0.209658179665771,2.5,4.3273098367647));
#170175=CARTESIAN_POINT('Ctrl Pts',(0.427502552552642,2.47160775999571,
4.37222300033197));
#170176=CARTESIAN_POINT('Ctrl Pts',(0.830717428883732,2.36749905155108,
4.54221720082959));
#170177=CARTESIAN_POINT('Ctrl Pts',(1.01472856346468,2.29060294533492,4.6704370541616));
#170178=CARTESIAN_POINT('Ctrl Pts',(1.30500271214396,2.13871416924791,4.96071120284089));
#170179=CARTESIAN_POINT('Ctrl Pts',(1.43214140343332,2.05201177715308,5.14433951978892));
#170180=CARTESIAN_POINT('Ctrl Pts',(1.60460561689046,1.92016237998017,5.55346129141822));
#170181=CARTESIAN_POINT('Ctrl Pts',(1.64999999999998,1.87816399709931,5.77993379108092));
#170182=CARTESIAN_POINT('Ctrl Pts',(1.64999999999998,1.87816399709931,5.99999999999999));
#170183=CARTESIAN_POINT('Ctrl Pts',(1.64999999999998,1.87816399709931,6.22029323766016));
#170184=CARTESIAN_POINT('Ctrl Pts',(1.60451571026845,1.92024797131867,6.44696680522557));
#170185=CARTESIAN_POINT('Ctrl Pts',(1.43174135154911,2.05230071367004,6.85639405508701));
#170186=CARTESIAN_POINT('Ctrl Pts',(1.30438035120314,2.13911407249231,7.04012885008982));
#170187=CARTESIAN_POINT('Ctrl Pts',(1.01388009229788,2.29097319034087,7.33019525229806));
#170188=CARTESIAN_POINT('Ctrl Pts',(0.829970933278287,2.36774524063037,
7.45818999174564));
#170189=CARTESIAN_POINT('Ctrl Pts',(0.418836606337158,2.473791677436,7.63133779833946));
#170190=CARTESIAN_POINT('Ctrl Pts',(0.191236948727583,2.50213878724098,
7.676167978));
#170191=CARTESIAN_POINT('Ctrl Pts',(-0.244986272291182,2.49757250522814,
7.676167978));
#170192=CARTESIAN_POINT('Ctrl Pts',(-0.473268510539828,2.46408580788034,
7.63080982181528));
#170193=CARTESIAN_POINT('Ctrl Pts',(-0.884756057426647,2.34795838069477,
7.45679987023969));
#170194=CARTESIAN_POINT('Ctrl Pts',(-1.06835830755764,2.26620995357749,
7.32849278967773));
#170195=CARTESIAN_POINT('Ctrl Pts',(-1.35766683964858,2.10579239001523,
7.03873339865919));
#170196=CARTESIAN_POINT('Ctrl Pts',(-1.48440903437884,2.01464276874607,
6.8556778229469));
#170197=CARTESIAN_POINT('Ctrl Pts',(-1.6566797985207,1.87554500871044,6.44730415212049));
#170198=CARTESIAN_POINT('Ctrl Pts',(-1.70233595600002,1.83086107963152,
6.22093525302607));
#170199=CARTESIAN_POINT('Ctrl Pts',(-1.70233595600002,1.83086107963151,
5.77906474697391));
#170200=CARTESIAN_POINT('Ctrl Pts',(-1.6566797985207,1.87554500871044,5.5526958478795));
#170201=CARTESIAN_POINT('Ctrl Pts',(-1.48440903437884,2.01464276874606,
5.14432217705309));
#170202=CARTESIAN_POINT('Ctrl Pts',(-1.35766683964858,2.10579239001523,
4.96126660134079));
#170203=CARTESIAN_POINT('Ctrl Pts',(-1.06835830755764,2.26620995357749,
4.67150721032225));
#170204=CARTESIAN_POINT('Ctrl Pts',(-0.884756057426646,2.34795838069477,
4.5432001297603));
#170205=CARTESIAN_POINT('Ctrl Pts',(-0.473268510539827,2.46408580788034,
4.3691901781847));
#170206=CARTESIAN_POINT('Ctrl Pts',(-0.244986272291182,2.49757250522813,
4.32383202199999));
#170207=CARTESIAN_POINT('Ctrl Pts',(-0.0261679780000215,2.49986304363407,
4.32383202199999));
#170208=CARTESIAN_POINT('Origin',(0.,1.22464679914735E-16,12.));
#170209=CARTESIAN_POINT('',(-2.4492935982947E-16,-2.,12.));
#170210=CARTESIAN_POINT('',(-2.44929359829471E-16,-2.,12.));
#170211=CARTESIAN_POINT('Origin',(0.,0.,12.));
#170212=CARTESIAN_POINT('Origin',(0.,1.22464679914735E-16,0.));
#170213=CARTESIAN_POINT('',(-2.,-1.22464679914735E-16,-7.27154827807832E-17));
#170214=CARTESIAN_POINT('',(-2.,-1.22464679914735E-16,0.));
#170215=CARTESIAN_POINT('Origin',(0.,0.,0.));
#170216=CARTESIAN_POINT('Origin',(-2.024,-2.024,0.));
#170217=CARTESIAN_POINT('Origin',(-2.024,-2.024,12.));
#170218=CARTESIAN_POINT('Origin',(-0.0261679780000106,-2.530830066,6.));
#170219=CARTESIAN_POINT('',(-0.0261679780000108,-2.53083006600001,4.323832022));
#170240=UNCERTAINTY_MEASURE_WITH_UNIT(LENGTH_MEASURE(0.01),#170251,
'DISTANCE_ACCURACY_VALUE',
'Maximum model space distance between geometric entities at asserted c
onnectivities');
#170242=UNCERTAINTY_MEASURE_WITH_UNIT(LENGTH_MEASURE(0.01),#170251,
'DISTANCE_ACCURACY_VALUE',
'Maximum model space distance between geometric entities at asserted c
onnectivities');
#170248=(
GEOMETRIC_REPRESENTATION_CONTEXT(3)
GLOBAL_UNCERTAINTY_ASSIGNED_CONTEXT((#170240))
GLOBAL_UNIT_ASSIGNED_CONTEXT((#170251,#170253,#170254))
REPRESENTATION_CONTEXT('','3D')
);
#170250=(
GEOMETRIC_REPRESENTATION_CONTEXT(3)
GLOBAL_UNCERTAINTY_ASSIGNED_CONTEXT((#170242))
GLOBAL_UNIT_ASSIGNED_CONTEXT((#170251,#170253,#170254))
REPRESENTATION_CONTEXT('','3D')
);
#170251=(
LENGTH_UNIT()
NAMED_UNIT(*)
SI_UNIT(.MILLI.,.METRE.)
);
#170253=(
NAMED_UNIT(*)
PLANE_ANGLE_UNIT()
SI_UNIT($,.RADIAN.)
);
#170254=(
NAMED_UNIT(*)
SI_UNIT($,.STERADIAN.)
SOLID_ANGLE_UNIT()
);
#170260=SHAPE_DEFINITION_REPRESENTATION(#170267,#170280);
#170267=PRODUCT_DEFINITION_SHAPE('',$,#170288);
#170280=SHAPE_REPRESENTATION('',(#77739),#170248);
#170282=PRODUCT_DEFINITION_CONTEXT('part definition',#170305,'design');
#170288=PRODUCT_DEFINITION('2026-11-14-09-55-10-334_4','Pin screw',#170295,
#170282);
#170295=PRODUCT_DEFINITION_FORMATION('',$,#170312);
#170305=APPLICATION_CONTEXT(
'Core Data for Automotive Mechanical Design Process');
#170306=PRODUCT_CONTEXT('part definition',#170305,'mechanical');
#170312=PRODUCT('2026-11-14-09-55-10-334_4','Pin screw',$,(#170306));
#170317=PRESENTATION_STYLE_ASSIGNMENT((#170321));
#170321=SURFACE_STYLE_USAGE(.BOTH.,#170325);
#170325=SURFACE_SIDE_STYLE('',(#170329));
#170329=SURFACE_STYLE_FILL_AREA(#170333);
#170333=FILL_AREA_STYLE('Opaque(31,36,43)',(#170337));
#170337=FILL_AREA_STYLE_COLOUR('Opaque(31,36,43)',#170341);
#170341=COLOUR_RGB('Opaque(31,36,43)',0.12156862745098,0.141176470588235,
0.168627450980392);
ENDSEC;
END-ISO-10303-21;
